ISO-10303-21;
HEADER;
/* Generated by software containing ST-Developer
 * from STEP Tools, Inc. (www.steptools.com) 
 */

FILE_DESCRIPTION(
/* description */ ('Grid plate located blocks and clamp'),
/* implementation_level */ '2;1');

FILE_NAME(
/* name */ 'Example round stock.step',
/* time_stamp */ '2026-10-29T15:43:47-07:00',
/* author */ (''),
/* organization */ (''),
/* preprocessor_version */ 'ST-DEVELOPER v20.2',
/* originating_system */ 'Autodesk Translation Framework v15.17.0.0',
/* authorisation */ '');

FILE_SCHEMA (('AUTOMOTIVE_DESIGN { 1 0 10303 214 3 1 1 }'));
ENDSEC;

DATA;
#10=MECHANICAL_DESIGN_GEOMETRIC_PRESENTATION_REPRESENTATION('',(#174),#5702);
#148=SHAPE_REPRESENTATION_RELATIONSHIP('SRR','None',#5766,#160);
#160=ADVANCED_BREP_SHAPE_REPRESENTATION('',(#187),#5696);
#174=STYLED_ITEM('',(#5890),#187);
#187=MANIFOLD_SOLID_BREP('Body1',#3270);
#352=CIRCLE('',#3629,1.5);
#353=CIRCLE('',#3630,1.5);
#437=CYLINDRICAL_SURFACE('',#3628,1.5);
#581=FACE_OUTER_BOUND('',#832,.T.);
#582=FACE_OUTER_BOUND('',#833,.T.);
#583=FACE_OUTER_BOUND('',#834,.T.);
#832=EDGE_LOOP('',(#2716,#2717,#2718,#2719));
#833=EDGE_LOOP('',(#2720));
#834=EDGE_LOOP('',(#2721));
#1105=LINE('',#5360,#1378);
#1378=VECTOR('',#4409,1.5);
#1635=VERTEX_POINT('',#5357);
#1636=VERTEX_POINT('',#5359);
#2008=EDGE_CURVE('',#1635,#1635,#352,.T.);
#2009=EDGE_CURVE('',#1635,#1636,#1105,.T.);
#2010=EDGE_CURVE('',#1636,#1636,#353,.T.);
#2716=ORIENTED_EDGE('',*,*,#2008,.F.);
#2717=ORIENTED_EDGE('',*,*,#2009,.T.);
#2718=ORIENTED_EDGE('',*,*,#2010,.T.);
#2719=ORIENTED_EDGE('',*,*,#2009,.F.);
#2720=ORIENTED_EDGE('',*,*,#2008,.T.);
#2721=ORIENTED_EDGE('',*,*,#2010,.F.);
#3044=PLANE('',#3631);
#3045=PLANE('',#3632);
#3202=ADVANCED_FACE('',(#581),#437,.T.);
#3203=ADVANCED_FACE('',(#582),#3044,.T.);
#3204=ADVANCED_FACE('',(#583),#3045,.F.);
#3270=CLOSED_SHELL('',(#3202,#3203,#3204));
#3627=AXIS2_PLACEMENT_3D('',#5355,#4403,#4404);
#3628=AXIS2_PLACEMENT_3D('',#5356,#4405,#4406);
#3629=AXIS2_PLACEMENT_3D('',#5358,#4407,#4408);
#3630=AXIS2_PLACEMENT_3D('',#5361,#4410,#4411);
#3631=AXIS2_PLACEMENT_3D('',#5362,#4412,#4413);
#3632=AXIS2_PLACEMENT_3D('',#5363,#4414,#4415);
#4403=DIRECTION('axis',(0.,0.,1.));
#4404=DIRECTION('refdir',(1.,0.,0.));
#4405=DIRECTION('center_axis',(1.,0.,0.));
#4406=DIRECTION('ref_axis',(0.,0.,-1.));
#4407=DIRECTION('center_axis',(1.,0.,0.));
#4408=DIRECTION('ref_axis',(0.,0.,-1.));
#4409=DIRECTION('',(-1.,0.,0.));
#4410=DIRECTION('center_axis',(1.,0.,0.));
#4411=DIRECTION('ref_axis',(0.,0.,-1.));
#4412=DIRECTION('center_axis',(1.,0.,0.));
#4413=DIRECTION('ref_axis',(0.,0.,-1.));
#4414=DIRECTION('center_axis',(1.,0.,0.));
#4415=DIRECTION('ref_axis',(0.,0.,-1.));
#5355=CARTESIAN_POINT('',(0.,0.,0.));
#5356=CARTESIAN_POINT('Origin',(3.,0.,4.62132034355964));
#5357=CARTESIAN_POINT('',(17.,-1.83697019872103E-16,6.12132034355964));
#5358=CARTESIAN_POINT('Origin',(17.,0.,4.62132034355964));
#5359=CARTESIAN_POINT('',(3.,-1.83697019872103E-16,6.12132034355964));
#5360=CARTESIAN_POINT('',(3.,-1.83697019872103E-16,6.12132034355964));
#5361=CARTESIAN_POINT('Origin',(3.,0.,4.62132034355964));
#5362=CARTESIAN_POINT('Origin',(17.,0.,4.62132034355964));
#5363=CARTESIAN_POINT('Origin',(3.,0.,4.62132034355964));
#5682=UNCERTAINTY_MEASURE_WITH_UNIT(LENGTH_MEASURE(0.001),#5703,
'DISTANCE_ACCURACY_VALUE',
'Maximum model space distance between geometric entities at asserted c
onnectivities');
#5688=UNCERTAINTY_MEASURE_WITH_UNIT(LENGTH_MEASURE(0.001),#5703,
'DISTANCE_ACCURACY_VALUE',
'Maximum model space distance between geometric entities at asserted c
onnectivities');
#5696=(
GEOMETRIC_REPRESENTATION_CONTEXT(3)
GLOBAL_UNCERTAINTY_ASSIGNED_CONTEXT((#5682))
GLOBAL_UNIT_ASSIGNED_CONTEXT((#5703,#5705,#5706))
REPRESENTATION_CONTEXT('','3D')
);
#5702=(
GEOMETRIC_REPRESENTATION_CONTEXT(3)
GLOBAL_UNCERTAINTY_ASSIGNED_CONTEXT((#5688))
GLOBAL_UNIT_ASSIGNED_CONTEXT((#5703,#5705,#5706))
REPRESENTATION_CONTEXT('','3D')
);
#5703=(
LENGTH_UNIT()
NAMED_UNIT(*)
SI_UNIT(.CENTI.,.METRE.)
);
#5705=(
NAMED_UNIT(*)
PLANE_ANGLE_UNIT()
SI_UNIT($,.RADIAN.)
);
#5706=(
NAMED_UNIT(*)
SI_UNIT($,.STERADIAN.)
SOLID_ANGLE_UNIT()
);
#5714=SHAPE_DEFINITION_REPRESENTATION(#5727,#5766);
#5727=PRODUCT_DEFINITION_SHAPE('',$,#5780);
#5766=SHAPE_REPRESENTATION('',(#3627),#5696);
#5772=PRODUCT_DEFINITION_CONTEXT('part definition',#5813,'design');
#5780=PRODUCT_DEFINITION('Example round stock',
'Example round stock',#5793,#5772);
#5793=PRODUCT_DEFINITION_FORMATION('',$,#5822);
#5813=APPLICATION_CONTEXT(
'Core Data for Automotive Mechanical Design Process');
#5814=PRODUCT_CONTEXT('part definition',#5813,'mechanical');
#5822=PRODUCT('Example round stock','Example round stock',
'Example round stock',(#5814));
#5884=COLOUR_RGB('Sky Blue',0.24,0.69,0.87);
#5885=FILL_AREA_STYLE_COLOUR('',#5884);
#5886=FILL_AREA_STYLE('',(#5885));
#5887=SURFACE_STYLE_FILL_AREA(#5886);
#5888=SURFACE_SIDE_STYLE('',(#5887));
#5889=SURFACE_STYLE_USAGE(.BOTH.,#5888);
#5890=PRESENTATION_STYLE_ASSIGNMENT((#5889));
ENDSEC;
END-ISO-10303-21;
